ISO-10303-21;
HEADER;
/* Generated by software containing ST-Developer
 * from STEP Tools, Inc. (www.steptools.com) 
 */
/* OPTION: using custom renumber hook */

FILE_DESCRIPTION(
/* description */ ('STEP AP242 Edition 2', 'CAx-IF Rec.Pracs.---Representation and Presentation of Product Manufa
cturing Information (PMI)---4.0---2014-10-13', 'CAx-IF Rec.Pracs.---3D Tessellated Geometry---0.4---2014-09-14', '2;1', 'CAx-IF Rec.Pracs.---User Defined Attributes---1.5---2016-08-15'),
/* implementation_level */ '2;1');

FILE_NAME(
/* name */ 'dip.step',
/* time_stamp */ '2026-10-08T12:15:07Z',
/* author */ (''),
/* organization */ (''),
/* preprocessor_version */ 'ST-DEVELOPER v20',
/* originating_system */ 'ONSHAPE BY PTC INC, 1.221',
/* authorisation */ '  ');

FILE_SCHEMA (('AP242_MANAGED_MODEL_BASED_3D_ENGINEERING_MIM_LF { 1 0 10303 442 3 1 4 }'));
ENDSEC;

DATA;
#60=COLOUR_RGB('', 0.66274510, 0.83137255, 0.94901961);
#213=SHAPE_REPRESENTATION_RELATIONSHIP('','',#13787,#240);
#240=ADVANCED_BREP_SHAPE_REPRESENTATION('',(#13731),#45477);
#747=CIRCLE('',#14643,0.00325);
#748=CIRCLE('',#14644,0.00375);
#749=CIRCLE('',#14646,0.00375);
#750=CIRCLE('',#14647,0.00325);
#1392=PLANE('',#14642);
#1393=PLANE('',#14645);
#1689=CYLINDRICAL_SURFACE('',#14648,0.00375);
#1690=CYLINDRICAL_SURFACE('',#14649,0.00325);
#4000=ORIENTED_EDGE('',*,*,#6647,.F.);
#4001=ORIENTED_EDGE('',*,*,#6648,.T.);
#4002=ORIENTED_EDGE('',*,*,#6649,.F.);
#4003=ORIENTED_EDGE('',*,*,#6650,.T.);
#4004=ORIENTED_EDGE('',*,*,#6648,.F.);
#4005=ORIENTED_EDGE('',*,*,#6649,.T.);
#4006=ORIENTED_EDGE('',*,*,#6647,.T.);
#4007=ORIENTED_EDGE('',*,*,#6650,.F.);
#6647=EDGE_CURVE('',#8184,#8184,#747,.T.);
#6648=EDGE_CURVE('',#8185,#8185,#748,.T.);
#6649=EDGE_CURVE('',#8186,#8186,#749,.T.);
#6650=EDGE_CURVE('',#8187,#8187,#750,.T.);
#8184=VERTEX_POINT('',#34958);
#8185=VERTEX_POINT('',#34960);
#8186=VERTEX_POINT('',#34963);
#8187=VERTEX_POINT('',#34965);
#11056=EDGE_LOOP('',(#4000));
#11057=EDGE_LOOP('',(#4001));
#11058=EDGE_LOOP('',(#4002));
#11059=EDGE_LOOP('',(#4003));
#11060=EDGE_LOOP('',(#4004));
#11061=EDGE_LOOP('',(#4005));
#11062=EDGE_LOOP('',(#4006));
#11063=EDGE_LOOP('',(#4007));
#12173=FACE_BOUND('',#11056,.T.);
#12174=FACE_BOUND('',#11057,.T.);
#12175=FACE_BOUND('',#11058,.T.);
#12176=FACE_BOUND('',#11059,.T.);
#12177=FACE_BOUND('',#11060,.T.);
#12178=FACE_BOUND('',#11061,.T.);
#12179=FACE_BOUND('',#11062,.T.);
#12180=FACE_BOUND('',#11063,.T.);
#13159=ADVANCED_FACE('',(#12173,#12174),#1392,.T.);
#13160=ADVANCED_FACE('',(#12175,#12176),#1393,.F.);
#13161=ADVANCED_FACE('',(#12177,#12178),#1689,.T.);
#13162=ADVANCED_FACE('',(#12179,#12180),#1690,.F.);
#13514=CLOSED_SHELL('',(#13159,#13160,#13161,#13162));
#13541=STYLED_ITEM('',(#13568),#13731);
#13568=PRESENTATION_STYLE_ASSIGNMENT((#13595));
#13595=SURFACE_STYLE_USAGE(.BOTH.,#13622);
#13622=SURFACE_SIDE_STYLE('',(#13649));
#13649=SURFACE_STYLE_FILL_AREA(#13676);
#13676=FILL_AREA_STYLE('',(#13703));
#13703=FILL_AREA_STYLE_COLOUR('',#60);
#13731=MANIFOLD_SOLID_BREP('dip',#13514);
#13759=SHAPE_DEFINITION_REPRESENTATION(#45550,#13787);
#13787=SHAPE_REPRESENTATION('dip',(#13802),#45477);
#13802=AXIS2_PLACEMENT_3D('',#19109,#15295,#15296);
#14642=AXIS2_PLACEMENT_3D('',#34956,#17449,#17450);
#14643=AXIS2_PLACEMENT_3D('',#34957,#17451,#17452);
#14644=AXIS2_PLACEMENT_3D('',#34959,#17453,#17454);
#14645=AXIS2_PLACEMENT_3D('',#34961,#17455,#17456);
#14646=AXIS2_PLACEMENT_3D('',#34962,#17457,#17458);
#14647=AXIS2_PLACEMENT_3D('',#34964,#17459,#17460);
#14648=AXIS2_PLACEMENT_3D('',#34966,#17461,#17462);
#14649=AXIS2_PLACEMENT_3D('',#34967,#17463,#17464);
#15295=DIRECTION('',(0.,0.,1.));
#15296=DIRECTION('',(1.,0.,0.));
#17449=DIRECTION('',(0.,0.,-1.));
#17450=DIRECTION('',(-1.,0.,0.));
#17451=DIRECTION('',(0.,0.,-1.));
#17452=DIRECTION('',(-1.,0.,0.));
#17453=DIRECTION('',(0.,0.,-1.));
#17454=DIRECTION('',(-1.,0.,0.));
#17455=DIRECTION('',(0.,0.,-1.));
#17456=DIRECTION('',(-1.,0.,0.));
#17457=DIRECTION('',(0.,0.,-1.));
#17458=DIRECTION('',(-1.,0.,0.));
#17459=DIRECTION('',(0.,0.,-1.));
#17460=DIRECTION('',(-1.,0.,0.));
#17461=DIRECTION('',(0.,0.,-1.));
#17462=DIRECTION('',(-1.,0.,0.));
#17463=DIRECTION('',(0.,0.,-1.));
#17464=DIRECTION('',(-1.,0.,0.));
#19109=CARTESIAN_POINT('',(0.,0.,0.));
#34956=CARTESIAN_POINT('',(0.,0.,-0.0620923697749146));
#34957=CARTESIAN_POINT('',(0.,0.,-0.0620923697749146));
#34958=CARTESIAN_POINT('',(-0.00325,0.,-0.0620923697749146));
#34959=CARTESIAN_POINT('',(0.,0.,-0.0620923697749146));
#34960=CARTESIAN_POINT('',(-0.00375,0.,-0.0620923697749146));
#34961=CARTESIAN_POINT('',(0.,0.,-0.0234923697749146));
#34962=CARTESIAN_POINT('',(0.,0.,-0.0234923697749146));
#34963=CARTESIAN_POINT('',(-0.00375,0.,-0.0234923697749146));
#34964=CARTESIAN_POINT('',(0.,0.,-0.0234923697749146));
#34965=CARTESIAN_POINT('',(-0.00325,0.,-0.0234923697749146));
#34966=CARTESIAN_POINT('',(0.,0.,-0.0234923697749146));
#34967=CARTESIAN_POINT('',(0.,0.,-0.0234923697749146));
#45463=MECHANICAL_DESIGN_GEOMETRIC_PRESENTATION_REPRESENTATION('',(#13541),#45464);
#45464=(
GEOMETRIC_REPRESENTATION_CONTEXT(3)
GLOBAL_UNCERTAINTY_ASSIGNED_CONTEXT((#45492))
GLOBAL_UNIT_ASSIGNED_CONTEXT((#45522,#45521,#45520))
REPRESENTATION_CONTEXT('MAS-690','TOP_LEVEL_ASSEMBLY_PART')
);
#45477=(
GEOMETRIC_REPRESENTATION_CONTEXT(3)
GLOBAL_UNCERTAINTY_ASSIGNED_CONTEXT((#45505))
GLOBAL_UNIT_ASSIGNED_CONTEXT((#45522,#45521,#45520))
REPRESENTATION_CONTEXT('dip','COMPONENT_PART')
);
#45492=UNCERTAINTY_MEASURE_WITH_UNIT(LENGTH_MEASURE(1.E-8),#45522,
'DISTANCE_ACCURACY_VALUE','Maximum Tolerance applied to model');
#45505=UNCERTAINTY_MEASURE_WITH_UNIT(LENGTH_MEASURE(1.E-8),#45522,
'DISTANCE_ACCURACY_VALUE','Maximum Tolerance applied to model');
#45520=(
NAMED_UNIT(*)
SI_UNIT($,.STERADIAN.)
SOLID_ANGLE_UNIT()
);
#45521=(
NAMED_UNIT(*)
PLANE_ANGLE_UNIT()
SI_UNIT($,.RADIAN.)
);
#45522=(
LENGTH_UNIT()
NAMED_UNIT(*)
SI_UNIT($,.METRE.)
);
#45550=PRODUCT_DEFINITION_SHAPE('','',#45598);
#45598=PRODUCT_DEFINITION('','',#45654,#45626);
#45626=PRODUCT_DEFINITION_CONTEXT('',#45782,'design');
#45654=PRODUCT_DEFINITION_FORMATION_WITH_SPECIFIED_SOURCE('','',#45710,
 .NOT_KNOWN.);
#45710=PRODUCT('dip','dip','dip',(#45766));
#45766=PRODUCT_CONTEXT('',#45782,'mechanical');
#45782=APPLICATION_CONTEXT('managed model based 3d engineering');
ENDSEC;
END-ISO-10303-21;
